ISO-10303-21;
HEADER;
FILE_DESCRIPTION (('STEP AP214'),
    '1' );
FILE_NAME ('spindle bearing.step',
    '2026-10-26T19:46:16',
    ( '' ),
    ( '' ),
    'SwSTEP 2.0',
    'SolidWorks 2025',
    '' );
FILE_SCHEMA (( 'AUTOMOTIVE_DESIGN' ));
ENDSEC;

DATA;
#119=AXIS2_PLACEMENT_3D ( 'NONE', #48713, #60410, #49084 ) ;
#451=CARTESIAN_POINT ( 'NONE',  ( 0.000000000000000000, 0.000000000000000000, 0.000000000000000000 ) ) ;
#622=ORIENTED_EDGE ( 'NONE', *, *, #15879, .T. ) ;
#639=DIRECTION ( 'NONE',  ( -1.000000000000000000, -0.000000000000000000, -0.000000000000000000 ) ) ;
#953=ORIENTED_EDGE ( 'NONE', *, *, #8192, .T. ) ;
#1178=VERTEX_POINT ( 'NONE', #69878 ) ;
#1266=EDGE_LOOP ( 'NONE', ( #5013, #66794 ) ) ;
#1383=LINE ( 'NONE', #63997, #11885 ) ;
#1464=CARTESIAN_POINT ( 'NONE',  ( 0.000000000000000000, 28.00000000000000000, 0.000000000000000000 ) ) ;
#1564=DIRECTION ( 'NONE',  ( 0.000000000000000000, 0.000000000000000000, 1.000000000000000000 ) ) ;
#1845=CARTESIAN_POINT ( 'NONE',  ( 12.00000000000000000, 0.000000000000000000, 0.000000000000000000 ) ) ;
#2049=CARTESIAN_POINT ( 'NONE',  ( 0.000000000000000000, 4.898587196589400010E-16, -24.00000000000001421 ) ) ;
#2107=CYLINDRICAL_SURFACE ( 'NONE', #21982, 3.999999999999986233 ) ;
#2337=AXIS2_PLACEMENT_3D ( 'NONE', #58900, #36251, #1564 ) ;
#2354=CIRCLE ( 'NONE', #28856, 3.999999999999988010 ) ;
#2417=ORIENTED_EDGE ( 'NONE', *, *, #55230, .T. ) ;
#2452=AXIS2_PLACEMENT_3D ( 'NONE', #68297, #23021, #46027 ) ;
#2479=FACE_OUTER_BOUND ( 'NONE', #62825, .T. ) ;
#2557=VECTOR ( 'NONE', #57714, 1000.000000000000000 ) ;
#2802=EDGE_CURVE ( 'NONE', #8416, #44642, #17133, .T. ) ;
#2961=EDGE_LOOP ( 'NONE', ( #72814, #30144, #61276, #43520 ) ) ;
#3209=CARTESIAN_POINT ( 'NONE',  ( 0.000000000000000000, -28.00000000000000000, -3.999999999999988010 ) ) ;
#3218=CARTESIAN_POINT ( 'NONE',  ( 0.000000000000000000, 0.000000000000000000, 0.000000000000000000 ) ) ;
#3282=DIRECTION ( 'NONE',  ( -1.000000000000000000, -0.000000000000000000, -0.000000000000000000 ) ) ;
#3607=AXIS2_PLACEMENT_3D ( 'NONE', #4342, #27711, #71864 ) ;
#3760=ORIENTED_EDGE ( 'NONE', *, *, #2802, .F. ) ;
#3794=EDGE_CURVE ( 'NONE', #47241, #6116, #20738, .T. ) ;
#3912=ADVANCED_FACE ( 'NONE', ( #49246 ), #27731, .F. ) ;
#3970=CIRCLE ( 'NONE', #62986, 3.999999999999986233 ) ;
#4045=DIRECTION ( 'NONE',  ( 0.000000000000000000, 0.000000000000000000, 1.000000000000000000 ) ) ;
#4342=CARTESIAN_POINT ( 'NONE',  ( 0.000000000000000000, 0.000000000000000000, 0.000000000000000000 ) ) ;
#4551=EDGE_CURVE ( 'NONE', #47128, #66240, #35390, .T. ) ;
#4582=DIRECTION ( 'NONE',  ( -1.000000000000000000, -0.000000000000000000, -0.000000000000000000 ) ) ;
#4658=ORIENTED_EDGE ( 'NONE', *, *, #50525, .F. ) ;
#5013=ORIENTED_EDGE ( 'NONE', *, *, #54714, .T. ) ;
#5287=FACE_BOUND ( 'NONE', #32571, .T. ) ;
#5448=CARTESIAN_POINT ( 'NONE',  ( 0.000000000000000000, 28.00000000000000000, -3.999999999999986233 ) ) ;
#5655=FACE_OUTER_BOUND ( 'NONE', #66520, .T. ) ;
#5660=CARTESIAN_POINT ( 'NONE',  ( 12.00000000000000000, 4.898587196589398038E-16, 31.99999999999998579 ) ) ;
#5769=DIRECTION ( 'NONE',  ( 0.000000000000000000, 0.000000000000000000, -1.000000000000000000 ) ) ;
#5945=VERTEX_POINT ( 'NONE', #44388 ) ;
#6116=VERTEX_POINT ( 'NONE', #64341 ) ;
#6144=ORIENTED_EDGE ( 'NONE', *, *, #62206, .F. ) ;
#6389=DIRECTION ( 'NONE',  ( -1.000000000000000000, -0.000000000000000000, -0.000000000000000000 ) ) ;
#6478=AXIS2_PLACEMENT_3D ( 'NONE', #44004, #72291, #20604 ) ;
#6489=EDGE_LOOP ( 'NONE', ( #30157, #953, #58750, #60205 ) ) ;
#6729=AXIS2_PLACEMENT_3D ( 'NONE', #11424, #62348, #5769 ) ;
#7034=VERTEX_POINT ( 'NONE', #18226 ) ;
#8064=ORIENTED_EDGE ( 'NONE', *, *, #72278, .F. ) ;
#8192=EDGE_CURVE ( 'NONE', #44095, #10770, #17206, .T. ) ;
#8265=CYLINDRICAL_SURFACE ( 'NONE', #21782, 3.999999999999986233 ) ;
#8383=CYLINDRICAL_SURFACE ( 'NONE', #66005, 9.999999999999996447 ) ;
#8410=CARTESIAN_POINT ( 'NONE',  ( 12.00000000000000178, -28.00000000000000000, 0.000000000000000000 ) ) ;
#8416=VERTEX_POINT ( 'NONE', #24714 ) ;
#8472=FACE_BOUND ( 'NONE', #36753, .T. ) ;
#8505=DIRECTION ( 'NONE',  ( 1.000000000000000000, -0.000000000000000000, -0.000000000000000000 ) ) ;
#8525=ADVANCED_BREP_SHAPE_REPRESENTATION ( '', ( #42707, #57354 ), #33286 ) ;
#8563=EDGE_LOOP ( 'NONE', ( #32698, #70702 ) ) ;
#8802=AXIS2_PLACEMENT_3D ( 'NONE', #72450, #44527, #21507 ) ;
#8852=EDGE_LOOP ( 'NONE', ( #74466, #4658 ) ) ;
#8926=DIRECTION ( 'NONE',  ( 0.000000000000000000, 0.000000000000000000, -1.000000000000000000 ) ) ;
#9166=DIRECTION ( 'NONE',  ( 0.000000000000000000, 0.000000000000000000, 1.000000000000000000 ) ) ;
#9607=FACE_BOUND ( 'NONE', #8852, .T. ) ;
#9689=CARTESIAN_POINT ( 'NONE',  ( 12.00000000000000178, -28.00000000000000000, 0.000000000000000000 ) ) ;
#10286=DIRECTION ( 'NONE',  ( 1.000000000000000000, -0.000000000000000000, -0.000000000000000000 ) ) ;
#10536=DIRECTION ( 'NONE',  ( 1.000000000000000000, -0.000000000000000000, -0.000000000000000000 ) ) ;
#10555=ORIENTED_EDGE ( 'NONE', *, *, #18102, .T. ) ;
#10770=VERTEX_POINT ( 'NONE', #27347 ) ;
#10805=AXIS2_PLACEMENT_3D ( 'NONE', #55254, #38267, #61271 ) ;
#11037=ADVANCED_FACE ( 'NONE', ( #36558 ), #25219, .F. ) ;
#11422=DIRECTION ( 'NONE',  ( 0.000000000000000000, 0.000000000000000000, 1.000000000000000000 ) ) ;
#11424=CARTESIAN_POINT ( 'NONE',  ( 17.99999999999999645, 0.000000000000000000, 19.00000000000000355 ) ) ;
#11462=FACE_OUTER_BOUND ( 'NONE', #28002, .T. ) ;
#11593=CIRCLE ( 'NONE', #18844, 19.00000000000000355 ) ;
#11650=EDGE_LOOP ( 'NONE', ( #33716, #34334, #23090, #26492 ) ) ;
#11720=CLOSED_SHELL ( 'NONE', ( #57920, #21422, #53345, #23794, #33069, #14802, #27539, #26325, #21847, #60599, #24559, #68848, #29143, #59130, #3912, #11037, #50058 ) ) ;
#11851=CIRCLE ( 'NONE', #34754, 19.00000000000000355 ) ;
#11880=UNCERTAINTY_MEASURE_WITH_UNIT (LENGTH_MEASURE( 1.000000000000000082E-05 ), #57835, 'distance_accuracy_value', 'NONE');
#11885=VECTOR ( 'NONE', #12312, 1000.000000000000000 ) ;
#11989=DIRECTION ( 'NONE',  ( 1.000000000000000000, -0.000000000000000000, -0.000000000000000000 ) ) ;
#12042=DIRECTION ( 'NONE',  ( -1.000000000000000000, -0.000000000000000000, -0.000000000000000000 ) ) ;
#12157=VECTOR ( 'NONE', #10536, 1000.000000000000000 ) ;
#12203=ORIENTED_EDGE ( 'NONE', *, *, #39052, .T. ) ;
#12299=EDGE_CURVE ( 'NONE', #7034, #42039, #72832, .T. ) ;
#12312=DIRECTION ( 'NONE',  ( -1.000000000000000000, -0.000000000000000000, -0.000000000000000000 ) ) ;
#12870=ORIENTED_EDGE ( 'NONE', *, *, #12299, .T. ) ;
#12884=PRODUCT_DEFINITION_FORMATION_WITH_SPECIFIED_SOURCE ( 'ANY', '', #62589, .NOT_KNOWN. ) ;
#13164=ORIENTED_EDGE ( 'NONE', *, *, #15516, .F. ) ;
#13327=CIRCLE ( 'NONE', #56771, 36.00000000000000000 ) ;
#13409=DIRECTION ( 'NONE',  ( 0.000000000000000000, 0.000000000000000000, -1.000000000000000000 ) ) ;
#13420=VECTOR ( 'NONE', #61382, 1000.000000000000000 ) ;
#13604=EDGE_LOOP ( 'NONE', ( #58259, #72327, #15956, #13164 ) ) ;
#13904=CYLINDRICAL_SURFACE ( 'NONE', #44463, 3.999999999999988010 ) ;
#13918=CARTESIAN_POINT ( 'NONE',  ( 12.00000000000000000, 28.00000000000000000, -3.999999999999986233 ) ) ;
#13939=APPLICATION_CONTEXT ( 'automotive_design' ) ;
#14350=ORIENTED_EDGE ( 'NONE', *, *, #33685, .F. ) ;
#14539=EDGE_CURVE ( 'NONE', #60403, #24263, #31684, .T. ) ;
#14802=ADVANCED_FACE ( 'NONE', ( #30568 ), #53588, .T. ) ;
#15005=EDGE_CURVE ( 'NONE', #5945, #42039, #39208, .T. ) ;
#15053=CARTESIAN_POINT ( 'NONE',  ( 0.000000000000000000, 0.000000000000000000, 24.00000000000001421 ) ) ;
#15082=LINE ( 'NONE', #38117, #66654 ) ;
#15181=ORIENTED_EDGE ( 'NONE', *, *, #43669, .T. ) ;
#15213=VERTEX_POINT ( 'NONE', #45605 ) ;
#15242=DIRECTION ( 'NONE',  ( 0.000000000000000000, 0.000000000000000000, 1.000000000000000000 ) ) ;
#15284=CARTESIAN_POINT ( 'NONE',  ( 12.00000000000000000, -28.00000000000000000, 0.000000000000000000 ) ) ;
#15333=CARTESIAN_POINT ( 'NONE',  ( 17.99999999999998934, 0.000000000000000000, 0.000000000000000000 ) ) ;
#15485=VERTEX_POINT ( 'NONE', #65169 ) ;
#15516=EDGE_CURVE ( 'NONE', #44642, #8416, #13327, .T. ) ;
#15879=EDGE_CURVE ( 'NONE', #47128, #15485, #29030, .T. ) ;
#15888=CARTESIAN_POINT ( 'NONE',  ( 0.000000000000000000, 0.000000000000000000, 0.000000000000000000 ) ) ;
#15928=DIRECTION ( 'NONE',  ( -1.000000000000000000, -0.000000000000000000, -0.000000000000000000 ) ) ;
#15956=ORIENTED_EDGE ( 'NONE', *, *, #57207, .T. ) ;
#16013=CYLINDRICAL_SURFACE ( 'NONE', #3607, 9.999999999999996447 ) ;
#16094=CARTESIAN_POINT ( 'NONE',  ( 0.000000000000000000, 4.408728476930470856E-15, -36.00000000000000000 ) ) ;
#16400=CARTESIAN_POINT ( 'NONE',  ( 12.00000000000000178, 4.898587196589402968E-16, 31.99999999999998579 ) ) ;
#16567=CARTESIAN_POINT ( 'NONE',  ( 12.00000000000000178, 0.000000000000000000, 28.00000000000000000 ) ) ;
#16965=ORIENTED_EDGE ( 'NONE', *, *, #23692, .T. ) ;
#16986=CARTESIAN_POINT ( 'NONE',  ( 0.000000000000000000, 0.000000000000000000, 0.000000000000000000 ) ) ;
#17099=ORIENTED_EDGE ( 'NONE', *, *, #27268, .F. ) ;
#17133=CIRCLE ( 'NONE', #23169, 36.00000000000000000 ) ;
#17206=LINE ( 'NONE', #62854, #38741 ) ;
#17275=CIRCLE ( 'NONE', #20871, 3.999999999999989786 ) ;
#17328=FACE_BOUND ( 'NONE', #68218, .T. ) ;
#17422=VERTEX_POINT ( 'NONE', #68808 ) ;
#17476=VERTEX_POINT ( 'NONE', #5448 ) ;
#17482=DIRECTION ( 'NONE',  ( 0.000000000000000000, 0.000000000000000000, -1.000000000000000000 ) ) ;
#17559=DIRECTION ( 'NONE',  ( 1.000000000000000000, -0.000000000000000000, -0.000000000000000000 ) ) ;
#17703=DIRECTION ( 'NONE',  ( -1.000000000000000000, 0.000000000000000000, -0.000000000000000000 ) ) ;
#17937=DIRECTION ( 'NONE',  ( 0.000000000000000000, 0.000000000000000000, -1.000000000000000000 ) ) ;
#17963=DIRECTION ( 'NONE',  ( 0.000000000000000000, 0.000000000000000000, 1.000000000000000000 ) ) ;
#17979=CIRCLE ( 'NONE', #24002, 3.999999999999989786 ) ;
#18102=EDGE_CURVE ( 'NONE', #15485, #47128, #23097, .T. ) ;
#18226=CARTESIAN_POINT ( 'NONE',  ( 12.00000000000000178, 28.00000000000000000, -3.999999999999986233 ) ) ;
#18451=DIRECTION ( 'NONE',  ( 0.000000000000000000, 0.000000000000000000, 1.000000000000000000 ) ) ;
#18770=ORIENTED_EDGE ( 'NONE', *, *, #18102, .F. ) ;
#18844=AXIS2_PLACEMENT_3D ( 'NONE', #60924, #48848, #66206 ) ;
#18908=DIRECTION ( 'NONE',  ( 0.000000000000000000, 0.000000000000000000, 1.000000000000000000 ) ) ;
#19075=DIRECTION ( 'NONE',  ( -1.000000000000000000, -0.000000000000000000, -0.000000000000000000 ) ) ;
#19591=( NAMED_UNIT ( * ) SI_UNIT ( $, .STERADIAN. ) SOLID_ANGLE_UNIT ( ) );
#19604=DIRECTION ( 'NONE',  ( -1.000000000000000000, -0.000000000000000000, -0.000000000000000000 ) ) ;
#19888=CARTESIAN_POINT ( 'NONE',  ( 0.000000000000000000, -28.00000000000000000, 0.000000000000000000 ) ) ;
#19931=DIRECTION ( 'NONE',  ( 0.000000000000000000, 0.000000000000000000, -1.000000000000000000 ) ) ;
#20102=EDGE_CURVE ( 'NONE', #5945, #17476, #47213, .T. ) ;
#20239=CARTESIAN_POINT ( 'NONE',  ( 0.000000000000000000, 0.000000000000000000, 0.000000000000000000 ) ) ;
#20253=DIRECTION ( 'NONE',  ( 0.000000000000000000, 0.000000000000000000, 1.000000000000000000 ) ) ;
#20328=EDGE_CURVE ( 'NONE', #48616, #44095, #56888, .T. ) ;
#20365=DIRECTION ( 'NONE',  ( 1.000000000000000000, -0.000000000000000000, -0.000000000000000000 ) ) ;
#20504=AXIS2_PLACEMENT_3D ( 'NONE', #15284, #20575, #67734 ) ;
#20575=DIRECTION ( 'NONE',  ( 1.000000000000000000, -0.000000000000000000, -0.000000000000000000 ) ) ;
#20604=DIRECTION ( 'NONE',  ( 0.000000000000000000, 0.000000000000000000, 1.000000000000000000 ) ) ;
#20642=VERTEX_POINT ( 'NONE', #2049 ) ;
#20738=CIRCLE ( 'NONE', #62907, 19.00000000000000355 ) ;
#20857=LINE ( 'NONE', #34446, #35376 ) ;
#20871=AXIS2_PLACEMENT_3D ( 'NONE', #16567, #39604, #8926 ) ;
#20877=CARTESIAN_POINT ( 'NONE',  ( 12.00000000000000000, 4.408728476930470856E-15, -36.00000000000000000 ) ) ;
#20975=VERTEX_POINT ( 'NONE', #20877 ) ;
#21071=EDGE_CURVE ( 'NONE', #61413, #36324, #56720, .T. ) ;
#21086=ORIENTED_EDGE ( 'NONE', *, *, #15879, .F. ) ;
#21180=FACE_OUTER_BOUND ( 'NONE', #45020, .T. ) ;
#21208=DIRECTION ( 'NONE',  ( -1.000000000000000000, -0.000000000000000000, -0.000000000000000000 ) ) ;
#21422=ADVANCED_FACE ( 'NONE', ( #43807 ), #31366, .F. ) ;
#21507=DIRECTION ( 'NONE',  ( 0.000000000000000000, 0.000000000000000000, -1.000000000000000000 ) ) ;
#21584=VECTOR ( 'NONE', #46755, 1000.000000000000000 ) ;
#21647=ORIENTED_EDGE ( 'NONE', *, *, #51176, .F. ) ;
#21694=ORIENTED_EDGE ( 'NONE', *, *, #60568, .F. ) ;
#21782=AXIS2_PLACEMENT_3D ( 'NONE', #25234, #42220, #37320 ) ;
#21838=DIRECTION ( 'NONE',  ( -1.000000000000000000, -0.000000000000000000, -0.000000000000000000 ) ) ;
#21847=ADVANCED_FACE ( 'NONE', ( #51325 ), #27191, .T. ) ;
#21982=AXIS2_PLACEMENT_3D ( 'NONE', #54543, #59460, #13409 ) ;
#22414=SHAPE_REPRESENTATION ( 'spindle bearing', ( #57354 ), #33286 ) ;
#22838=PRODUCT_DEFINITION_SHAPE ( 'NONE', 'NONE',  #67598 ) ;
#22936=PRODUCT_CONTEXT ( 'NONE', #27400, 'mechanical' ) ;
#22972=EDGE_LOOP ( 'NONE', ( #48247, #58271, #56529, #54573 ) ) ;
#23021=DIRECTION ( 'NONE',  ( 1.000000000000000000, -0.000000000000000000, -0.000000000000000000 ) ) ;
#23081=ORIENTED_EDGE ( 'NONE', *, *, #35269, .F. ) ;
#23090=ORIENTED_EDGE ( 'NONE', *, *, #62693, .T. ) ;
#23097=CIRCLE ( 'NONE', #73717, 3.999999999999986233 ) ;
#23122=ORIENTED_EDGE ( 'NONE', *, *, #23692, .F. ) ;
#23169=AXIS2_PLACEMENT_3D ( 'NONE', #32566, #15928, #9166 ) ;
#23692=EDGE_CURVE ( 'NONE', #60403, #61413, #73166, .T. ) ;
#23794=ADVANCED_FACE ( 'NONE', ( #11462 ), #57503, .F. ) ;
#23956=CIRCLE ( 'NONE', #63708, 3.999999999999986233 ) ;
#24002=AXIS2_PLACEMENT_3D ( 'NONE', #9689, #72300, #50410 ) ;
#24044=CIRCLE ( 'NONE', #2337, 9.999999999999996447 ) ;
#24263=VERTEX_POINT ( 'NONE', #40046 ) ;
#24445=DIRECTION ( 'NONE',  ( -1.000000000000000000, -0.000000000000000000, -0.000000000000000000 ) ) ;
#24559=ADVANCED_FACE ( 'NONE', ( #30574 ), #41526, .T. ) ;
#24689=CARTESIAN_POINT ( 'NONE',  ( 12.00000000000000178, 28.00000000000000000, 0.000000000000000000 ) ) ;
#24714=CARTESIAN_POINT ( 'NONE',  ( 0.000000000000000000, 0.000000000000000000, 36.00000000000000000 ) ) ;
#24875=DIRECTION ( 'NONE',  ( 1.000000000000000000, -0.000000000000000000, -0.000000000000000000 ) ) ;
#24887=AXIS2_PLACEMENT_3D ( 'NONE', #49080, #71716, #60405 ) ;
#25158=DIRECTION ( 'NONE',  ( 0.000000000000000000, 0.000000000000000000, 1.000000000000000000 ) ) ;
#25219=CYLINDRICAL_SURFACE ( 'NONE', #52331, 3.999999999999986233 ) ;
#25234=CARTESIAN_POINT ( 'NONE',  ( 12.00000000000000000, 0.000000000000000000, 28.00000000000000000 ) ) ;
#26227=ORIENTED_EDGE ( 'NONE', *, *, #37588, .F. ) ;
#26325=ADVANCED_FACE ( 'NONE', ( #34345, #57344, #5287, #17328, #5655, #28654 ), #62608, .T. ) ;
#26372=DIRECTION ( 'NONE',  ( 0.000000000000000000, 0.000000000000000000, 1.000000000000000000 ) ) ;
#26492=ORIENTED_EDGE ( 'NONE', *, *, #54048, .T. ) ;
#26501=ORIENTED_EDGE ( 'NONE', *, *, #55230, .F. ) ;
#26747=AXIS2_PLACEMENT_3D ( 'NONE', #19888, #71941, #20253 ) ;
#26913=CARTESIAN_POINT ( 'NONE',  ( 12.00000000000000178, 0.000000000000000000, 24.00000000000001066 ) ) ;
#27191=CYLINDRICAL_SURFACE ( 'NONE', #62272, 36.00000000000000000 ) ;
#27268=EDGE_CURVE ( 'NONE', #6116, #1178, #70514, .T. ) ;
#27281=DIRECTION ( 'NONE',  ( -1.000000000000000000, -0.000000000000000000, -0.000000000000000000 ) ) ;
#27347=CARTESIAN_POINT ( 'NONE',  ( 12.00000000000000178, -28.00000000000000000, 3.999999999999989786 ) ) ;
#27400=APPLICATION_CONTEXT ( 'automotive_design' ) ;
#27539=ADVANCED_FACE ( 'NONE', ( #21180 ), #67592, .T. ) ;
#27619=AXIS2_PLACEMENT_3D ( 'NONE', #41096, #17703, #69766 ) ;
#27711=DIRECTION ( 'NONE',  ( -1.000000000000000000, -0.000000000000000000, -0.000000000000000000 ) ) ;
#27731=CYLINDRICAL_SURFACE ( 'NONE', #20504, 3.999999999999988010 ) ;
#27788=LINE ( 'NONE', #55364, #13420 ) ;
#28002=EDGE_LOOP ( 'NONE', ( #622, #57631, #12203, #52962 ) ) ;
#28072=ORIENTED_EDGE ( 'NONE', *, *, #50100, .T. ) ;
#28109=EDGE_LOOP ( 'NONE', ( #73237, #23122, #45724, #33603 ) ) ;
#28148=EDGE_CURVE ( 'NONE', #44095, #48616, #2354, .T. ) ;
#28392=ORIENTED_EDGE ( 'NONE', *, *, #63054, .F. ) ;
#28654=FACE_BOUND ( 'NONE', #29870, .T. ) ;
#28675=FACE_OUTER_BOUND ( 'NONE', #52543, .T. ) ;
#28752=AXIS2_PLACEMENT_3D ( 'NONE', #20239, #3282, #25158 ) ;
#28803=CARTESIAN_POINT ( 'NONE',  ( 12.00000000000000000, 0.000000000000000000, 28.00000000000000000 ) ) ;
#28856=AXIS2_PLACEMENT_3D ( 'NONE', #45988, #6389, #69750 ) ;
#28985=VECTOR ( 'NONE', #11989, 1000.000000000000000 ) ;
#29030=CIRCLE ( 'NONE', #72363, 3.999999999999986233 ) ;
#29052=CARTESIAN_POINT ( 'NONE',  ( 12.00000000000000178, 0.000000000000000000, 28.00000000000000000 ) ) ;
#29143=ADVANCED_FACE ( 'NONE', ( #33032 ), #16013, .F. ) ;
#29149=FACE_BOUND ( 'NONE', #71406, .T. ) ;
#29520=PLANE ( 'NONE',  #6729 ) ;
#29769=DIRECTION ( 'NONE',  ( -1.000000000000000000, -0.000000000000000000, -0.000000000000000000 ) ) ;
#29870=EDGE_LOOP ( 'NONE', ( #23081, #6144 ) ) ;
#30144=ORIENTED_EDGE ( 'NONE', *, *, #27268, .T. ) ;
#30157=ORIENTED_EDGE ( 'NONE', *, *, #20328, .T. ) ;
#30568=FACE_OUTER_BOUND ( 'NONE', #2961, .T. ) ;
#30574=FACE_OUTER_BOUND ( 'NONE', #36028, .T. ) ;
#30905=FACE_OUTER_BOUND ( 'NONE', #6489, .T. ) ;
#31113=MECHANICAL_DESIGN_GEOMETRIC_PRESENTATION_REPRESENTATION('',(#72086),#70906);
#31168=CIRCLE ( 'NONE', #28752, 9.999999999999996447 ) ;
#31366=CYLINDRICAL_SURFACE ( 'NONE', #24887, 3.999999999999986233 ) ;
#31439=AXIS2_PLACEMENT_3D ( 'NONE', #53953, #21838, #26372 ) ;
#31492=CARTESIAN_POINT ( 'NONE',  ( 12.00000000000000178, 0.000000000000000000, -28.00000000000000000 ) ) ;
#31684=LINE ( 'NONE', #66002, #37405 ) ;
#31756=AXIS2_PLACEMENT_3D ( 'NONE', #3218, #19075, #65089 ) ;
#32352=CARTESIAN_POINT ( 'NONE',  ( 0.000000000000000000, 0.000000000000000000, 0.000000000000000000 ) ) ;
#32566=CARTESIAN_POINT ( 'NONE',  ( 0.000000000000000000, 0.000000000000000000, 0.000000000000000000 ) ) ;
#32571=EDGE_LOOP ( 'NONE', ( #69234, #60639 ) ) ;
#32631=CIRCLE ( 'NONE', #119, 36.00000000000000000 ) ;
#32698=ORIENTED_EDGE ( 'NONE', *, *, #63063, .F. ) ;
#32721=DIRECTION ( 'NONE',  ( -1.000000000000000000, -0.000000000000000000, -0.000000000000000000 ) ) ;
#33032=FACE_OUTER_BOUND ( 'NONE', #28109, .T. ) ;
#33069=ADVANCED_FACE ( 'NONE', ( #60062 ), #8383, .F. ) ;
#33159=EDGE_LOOP ( 'NONE', ( #66090, #15181, #73274, #48010 ) ) ;
#33246=PRODUCT_DEFINITION_CONTEXT ( 'detailed design', #13939, 'design' ) ;
#33286=( GEOMETRIC_REPRESENTATION_CONTEXT ( 3 ) GLOBAL_UNCERTAINTY_ASSIGNED_CONTEXT ( ( #11880 ) ) GLOBAL_UNIT_ASSIGNED_CONTEXT ( ( #57835, #52164, #46488 ) ) REPRESENTATION_CONTEXT ( 'NONE', 'WORKASPACE' ) );
#33603=ORIENTED_EDGE ( 'NONE', *, *, #35269, .T. ) ;
#33680=AXIS2_PLACEMENT_3D ( 'NONE', #15888, #39289, #62290 ) ;
#33685=EDGE_CURVE ( 'NONE', #1178, #45978, #11851, .T. ) ;
#33716=ORIENTED_EDGE ( 'NONE', *, *, #8192, .F. ) ;
#34334=ORIENTED_EDGE ( 'NONE', *, *, #28148, .T. ) ;
#34345=FACE_BOUND ( 'NONE', #8563, .T. ) ;
#34446=CARTESIAN_POINT ( 'NONE',  ( 0.000000000000000000, 4.408728476930470856E-15, -36.00000000000000000 ) ) ;
#34459=DIRECTION ( 'NONE',  ( 1.000000000000000000, 0.000000000000000000, 0.000000000000000000 ) ) ;
#34654=SHAPE_DEFINITION_REPRESENTATION ( #22838, #22414 ) ;
#34754=AXIS2_PLACEMENT_3D ( 'NONE', #36541, #12042, #47477 ) ;
#34806=DIRECTION ( 'NONE',  ( -1.000000000000000000, -0.000000000000000000, -0.000000000000000000 ) ) ;
#34811=ORIENTED_EDGE ( 'NONE', *, *, #36176, .F. ) ;
#35102=CYLINDRICAL_SURFACE ( 'NONE', #2452, 3.999999999999986233 ) ;
#35177=ORIENTED_EDGE ( 'NONE', *, *, #58738, .F. ) ;
#35269=EDGE_CURVE ( 'NONE', #24263, #36324, #31168, .T. ) ;
#35376=VECTOR ( 'NONE', #74031, 1000.000000000000000 ) ;
#35390=LINE ( 'NONE', #40661, #28985 ) ;
#35395=CIRCLE ( 'NONE', #31756, 9.999999999999996447 ) ;
#35508=DIRECTION ( 'NONE',  ( 0.000000000000000000, 0.000000000000000000, 1.000000000000000000 ) ) ;
#35556=SHAPE_REPRESENTATION_RELATIONSHIP ( 'NONE' , 'NONE' ,  #22414, #8525 ) ;
#36012=CIRCLE ( 'NONE', #48004, 3.999999999999986233 ) ;
#36028=EDGE_LOOP ( 'NONE', ( #17099, #69050, #71052, #14350 ) ) ;
#36176=EDGE_CURVE ( 'NONE', #6116, #47241, #11593, .T. ) ;
#36180=VECTOR ( 'NONE', #4582, 1000.000000000000000 ) ;
#36251=DIRECTION ( 'NONE',  ( -1.000000000000000000, -0.000000000000000000, -0.000000000000000000 ) ) ;
#36324=VERTEX_POINT ( 'NONE', #48388 ) ;
#36541=CARTESIAN_POINT ( 'NONE',  ( 11.99999999999999822, 0.000000000000000000, 0.000000000000000000 ) ) ;
#36558=FACE_OUTER_BOUND ( 'NONE', #33159, .T. ) ;
#36753=EDGE_LOOP ( 'NONE', ( #72941, #68000 ) ) ;
#37001=CIRCLE ( 'NONE', #61125, 3.999999999999989786 ) ;
#37094=ORIENTED_EDGE ( 'NONE', *, *, #63063, .T. ) ;
#37148=FACE_BOUND ( 'NONE', #51409, .T. ) ;
#37318=DIRECTION ( 'NONE',  ( 1.000000000000000000, -0.000000000000000000, -0.000000000000000000 ) ) ;
#37320=DIRECTION ( 'NONE',  ( 0.000000000000000000, 0.000000000000000000, -1.000000000000000000 ) ) ;
#37405=VECTOR ( 'NONE', #19604, 1000.000000000000000 ) ;
#37588=EDGE_CURVE ( 'NONE', #17422, #20975, #63440, .T. ) ;
#38065=EDGE_CURVE ( 'NONE', #15485, #64014, #67912, .T. ) ;
#38117=CARTESIAN_POINT ( 'NONE',  ( 12.00000000000000000, -28.00000000000000000, -3.999999999999988010 ) ) ;
#38267=DIRECTION ( 'NONE',  ( -1.000000000000000000, -0.000000000000000000, -0.000000000000000000 ) ) ;
#38275=PLANE ( 'NONE',  #73328 ) ;
#38741=VECTOR ( 'NONE', #47363, 1000.000000000000000 ) ;
#39052=EDGE_CURVE ( 'NONE', #64014, #66240, #37001, .T. ) ;
#39208=LINE ( 'NONE', #62210, #12157 ) ;
#39289=DIRECTION ( 'NONE',  ( -1.000000000000000000, -0.000000000000000000, -0.000000000000000000 ) ) ;
#39604=DIRECTION ( 'NONE',  ( 1.000000000000000000, -0.000000000000000000, -0.000000000000000000 ) ) ;
#40013=DIRECTION ( 'NONE',  ( -1.000000000000000000, -0.000000000000000000, -0.000000000000000000 ) ) ;
#40046=CARTESIAN_POINT ( 'NONE',  ( 0.000000000000000000, 0.000000000000000000, 9.999999999999996447 ) ) ;
#40088=AXIS2_PLACEMENT_3D ( 'NONE', #8410, #10286, #49137 ) ;
#40357=DIRECTION ( 'NONE',  ( 1.000000000000000000, -0.000000000000000000, -0.000000000000000000 ) ) ;
#40661=CARTESIAN_POINT ( 'NONE',  ( 12.00000000000000000, 0.000000000000000000, 24.00000000000001421 ) ) ;
#40796=ORIENTED_EDGE ( 'NONE', *, *, #43669, .F. ) ;
#41096=CARTESIAN_POINT ( 'NONE',  ( 0.000000000000000000, 0.000000000000000000, 9.999999999999996447 ) ) ;
#41447=CARTESIAN_POINT ( 'NONE',  ( 0.000000000000000000, 0.000000000000000000, -31.99999999999998579 ) ) ;
#41495=FACE_OUTER_BOUND ( 'NONE', #48392, .T. ) ;
#41526=CYLINDRICAL_SURFACE ( 'NONE', #70853, 19.00000000000000355 ) ;
#41592=ORIENTED_EDGE ( 'NONE', *, *, #15005, .F. ) ;
#41673=EDGE_LOOP ( 'NONE', ( #48952, #34811 ) ) ;
#41857=CARTESIAN_POINT ( 'NONE',  ( 12.00000000000000000, -28.00000000000000000, 0.000000000000000000 ) ) ;
#42039=VERTEX_POINT ( 'NONE', #55274 ) ;
#42220=DIRECTION ( 'NONE',  ( 1.000000000000000000, -0.000000000000000000, -0.000000000000000000 ) ) ;
#42704=AXIS2_PLACEMENT_3D ( 'NONE', #24689, #17559, #17937 ) ;
#42707=MANIFOLD_SOLID_BREP ( '\X2\00d8\X0\8.0mm Dowel Hole1', #11720 ) ;
#42763=EDGE_CURVE ( 'NONE', #17476, #7034, #69813, .T. ) ;
#42810=VERTEX_POINT ( 'NONE', #47157 ) ;
#43128=ORIENTED_EDGE ( 'NONE', *, *, #63054, .T. ) ;
#43520=ORIENTED_EDGE ( 'NONE', *, *, #61981, .F. ) ;
#43540=DIRECTION ( 'NONE',  ( 1.000000000000000000, -0.000000000000000000, -0.000000000000000000 ) ) ;
#43669=EDGE_CURVE ( 'NONE', #20642, #44181, #23956, .T. ) ;
#43807=FACE_OUTER_BOUND ( 'NONE', #22972, .T. ) ;
#43927=FACE_BOUND ( 'NONE', #60546, .T. ) ;
#44004=CARTESIAN_POINT ( 'NONE',  ( 0.000000000000000000, 28.00000000000000000, 0.000000000000000000 ) ) ;
#44095=VERTEX_POINT ( 'NONE', #65556 ) ;
#44167=AXIS2_PLACEMENT_3D ( 'NONE', #1845, #29769, #18451 ) ;
#44181=VERTEX_POINT ( 'NONE', #41447 ) ;
#44196=CARTESIAN_POINT ( 'NONE',  ( 0.000000000000000000, 0.000000000000000000, 36.00000000000000000 ) ) ;
#44388=CARTESIAN_POINT ( 'NONE',  ( 0.000000000000000000, 28.00000000000000000, 3.999999999999986233 ) ) ;
#44463=AXIS2_PLACEMENT_3D ( 'NONE', #41857, #37318, #48991 ) ;
#44527=DIRECTION ( 'NONE',  ( 1.000000000000000000, -0.000000000000000000, -0.000000000000000000 ) ) ;
#44642=VERTEX_POINT ( 'NONE', #16094 ) ;
#44896=CIRCLE ( 'NONE', #40088, 3.999999999999989786 ) ;
#45020=EDGE_LOOP ( 'NONE', ( #46033, #58756, #3760, #52970 ) ) ;
#45426=CARTESIAN_POINT ( 'NONE',  ( 0.000000000000000000, 0.000000000000000000, -28.00000000000000000 ) ) ;
#45458=ORIENTED_EDGE ( 'NONE', *, *, #38065, .F. ) ;
#45605=CARTESIAN_POINT ( 'NONE',  ( 12.00000000000000178, -28.00000000000000000, -3.999999999999989786 ) ) ;
#45724=ORIENTED_EDGE ( 'NONE', *, *, #14539, .T. ) ;
#45739=EDGE_CURVE ( 'NONE', #44181, #42810, #51664, .T. ) ;
#45748=FACE_OUTER_BOUND ( 'NONE', #41673, .T. ) ;
#45762=VERTEX_POINT ( 'NONE', #65192 ) ;
#45779=ORIENTED_EDGE ( 'NONE', *, *, #2802, .T. ) ;
#45976=DIRECTION ( 'NONE',  ( 0.000000000000000000, 0.000000000000000000, 1.000000000000000000 ) ) ;
#45978=VERTEX_POINT ( 'NONE', #72351 ) ;
#45988=CARTESIAN_POINT ( 'NONE',  ( 0.000000000000000000, -28.00000000000000000, 0.000000000000000000 ) ) ;
#46027=DIRECTION ( 'NONE',  ( 0.000000000000000000, 0.000000000000000000, -1.000000000000000000 ) ) ;
#46033=ORIENTED_EDGE ( 'NONE', *, *, #37588, .T. ) ;
#46174=DIRECTION ( 'NONE',  ( 0.000000000000000000, 0.000000000000000000, 1.000000000000000000 ) ) ;
#46444=DIRECTION ( 'NONE',  ( -1.000000000000000000, -0.000000000000000000, -0.000000000000000000 ) ) ;
#46488=( NAMED_UNIT ( * ) SI_UNIT ( $, .STERADIAN. ) SOLID_ANGLE_UNIT ( ) );
#46755=DIRECTION ( 'NONE',  ( -1.000000000000000000, -0.000000000000000000, -0.000000000000000000 ) ) ;
#47124=CARTESIAN_POINT ( 'NONE',  ( 0.000000000000000000, 2.326828918379971365E-15, -19.00000000000000355 ) ) ;
#47128=VERTEX_POINT ( 'NONE', #15053 ) ;
#47157=CARTESIAN_POINT ( 'NONE',  ( 12.00000000000000178, 0.000000000000000000, -31.99999999999998579 ) ) ;
#47213=CIRCLE ( 'NONE', #62897, 3.999999999999986233 ) ;
#47241=VERTEX_POINT ( 'NONE', #50789 ) ;
#47363=DIRECTION ( 'NONE',  ( 1.000000000000000000, -0.000000000000000000, -0.000000000000000000 ) ) ;
#47477=DIRECTION ( 'NONE',  ( 0.000000000000000000, 0.000000000000000000, 1.000000000000000000 ) ) ;
#47955=EDGE_CURVE ( 'NONE', #20642, #45762, #27788, .T. ) ;
#48004=AXIS2_PLACEMENT_3D ( 'NONE', #31492, #43540, #54514 ) ;
#48010=ORIENTED_EDGE ( 'NONE', *, *, #60568, .T. ) ;
#48234=DIRECTION ( 'NONE',  ( 1.000000000000000000, -0.000000000000000000, -0.000000000000000000 ) ) ;
#48247=ORIENTED_EDGE ( 'NONE', *, *, #72278, .T. ) ;
#48388=CARTESIAN_POINT ( 'NONE',  ( 0.000000000000000000, 1.224646799147352862E-15, -9.999999999999996447 ) ) ;
#48392=EDGE_LOOP ( 'NONE', ( #45458, #10555, #63111, #43128 ) ) ;
#48616=VERTEX_POINT ( 'NONE', #3209 ) ;
#48685=EDGE_LOOP ( 'NONE', ( #26501, #56167, #72549, #61815 ) ) ;
#48713=CARTESIAN_POINT ( 'NONE',  ( 12.00000000000000000, 0.000000000000000000, 0.000000000000000000 ) ) ;
#48829=DIRECTION ( 'NONE',  ( 0.000000000000000000, 0.000000000000000000, -1.000000000000000000 ) ) ;
#48848=DIRECTION ( 'NONE',  ( -1.000000000000000000, -0.000000000000000000, -0.000000000000000000 ) ) ;
#48858=CARTESIAN_POINT ( 'NONE',  ( 12.00000000000000178, 28.00000000000000000, 0.000000000000000000 ) ) ;
#48952=ORIENTED_EDGE ( 'NONE', *, *, #3794, .F. ) ;
#48991=DIRECTION ( 'NONE',  ( 0.000000000000000000, 0.000000000000000000, -1.000000000000000000 ) ) ;
#49080=CARTESIAN_POINT ( 'NONE',  ( 12.00000000000000000, 0.000000000000000000, -28.00000000000000000 ) ) ;
#49084=DIRECTION ( 'NONE',  ( 0.000000000000000000, 0.000000000000000000, 1.000000000000000000 ) ) ;
#49137=DIRECTION ( 'NONE',  ( 0.000000000000000000, 0.000000000000000000, -1.000000000000000000 ) ) ;
#49246=FACE_OUTER_BOUND ( 'NONE', #11650, .T. ) ;
#49348=CIRCLE ( 'NONE', #10805, 19.00000000000000355 ) ;
#49871=DIRECTION ( 'NONE',  ( -1.000000000000000000, -0.000000000000000000, -0.000000000000000000 ) ) ;
#50058=ADVANCED_FACE ( 'NONE', ( #2479 ), #2107, .F. ) ;
#50100=EDGE_CURVE ( 'NONE', #42039, #7034, #3970, .T. ) ;
#50410=DIRECTION ( 'NONE',  ( 0.000000000000000000, 0.000000000000000000, -1.000000000000000000 ) ) ;
#50525=EDGE_CURVE ( 'NONE', #10770, #15213, #44896, .T. ) ;
#50789=CARTESIAN_POINT ( 'NONE',  ( 18.00000000000000000, 0.000000000000000000, 19.00000000000000355 ) ) ;
#51176=EDGE_CURVE ( 'NONE', #45762, #42810, #66621, .T. ) ;
#51325=FACE_OUTER_BOUND ( 'NONE', #13604, .T. ) ;
#51409=EDGE_LOOP ( 'NONE', ( #28392, #54439 ) ) ;
#51457=AXIS2_PLACEMENT_3D ( 'NONE', #15333, #32721, #4045 ) ;
#51664=LINE ( 'NONE', #56596, #2557 ) ;
#51690=DIRECTION ( 'NONE',  ( 1.000000000000000000, -0.000000000000000000, -0.000000000000000000 ) ) ;
#51821=DIRECTION ( 'NONE',  ( 1.000000000000000000, -0.000000000000000000, -0.000000000000000000 ) ) ;
#52164=( NAMED_UNIT ( * ) PLANE_ANGLE_UNIT ( ) SI_UNIT ( $, .RADIAN. ) );
#52244=CIRCLE ( 'NONE', #6478, 3.999999999999986233 ) ;
#52303=CARTESIAN_POINT ( 'NONE',  ( 0.000000000000000000, 0.000000000000000000, 28.00000000000000000 ) ) ;
#52331=AXIS2_PLACEMENT_3D ( 'NONE', #59572, #48234, #19931 ) ;
#52543=EDGE_LOOP ( 'NONE', ( #37094, #63805, #28072, #60838 ) ) ;
#52568=EDGE_CURVE ( 'NONE', #20975, #44642, #20857, .T. ) ;
#52621=VECTOR ( 'NONE', #40357, 1000.000000000000000 ) ;
#52962=ORIENTED_EDGE ( 'NONE', *, *, #4551, .F. ) ;
#52970=ORIENTED_EDGE ( 'NONE', *, *, #57207, .F. ) ;
#53345=ADVANCED_FACE ( 'NONE', ( #30905 ), #13904, .F. ) ;
#53588=CYLINDRICAL_SURFACE ( 'NONE', #31439, 19.00000000000000355 ) ;
#53764=EDGE_LOOP ( 'NONE', ( #26227, #35177 ) ) ;
#53953=CARTESIAN_POINT ( 'NONE',  ( 0.000000000000000000, 0.000000000000000000, 0.000000000000000000 ) ) ;
#54048=EDGE_CURVE ( 'NONE', #15213, #10770, #17979, .T. ) ;
#54439=ORIENTED_EDGE ( 'NONE', *, *, #39052, .F. ) ;
#54514=DIRECTION ( 'NONE',  ( 0.000000000000000000, 0.000000000000000000, -1.000000000000000000 ) ) ;
#54543=CARTESIAN_POINT ( 'NONE',  ( 12.00000000000000000, 28.00000000000000000, 0.000000000000000000 ) ) ;
#54573=ORIENTED_EDGE ( 'NONE', *, *, #45739, .F. ) ;
#54714=EDGE_CURVE ( 'NONE', #45978, #1178, #49348, .T. ) ;
#55230=EDGE_CURVE ( 'NONE', #61413, #60403, #24044, .T. ) ;
#55254=CARTESIAN_POINT ( 'NONE',  ( 11.99999999999999822, 0.000000000000000000, 0.000000000000000000 ) ) ;
#55268=VECTOR ( 'NONE', #24875, 1000.000000000000000 ) ;
#55274=CARTESIAN_POINT ( 'NONE',  ( 12.00000000000000178, 28.00000000000000000, 3.999999999999986233 ) ) ;
#55364=CARTESIAN_POINT ( 'NONE',  ( 12.00000000000000000, 4.898587196589398038E-16, -24.00000000000001421 ) ) ;
#55635=DIRECTION ( 'NONE',  ( 1.000000000000000000, 0.000000000000000000, 0.000000000000000000 ) ) ;
#56006=FACE_BOUND ( 'NONE', #1266, .T. ) ;
#56167=ORIENTED_EDGE ( 'NONE', *, *, #21071, .T. ) ;
#56264=LINE ( 'NONE', #44196, #36180 ) ;
#56300=CARTESIAN_POINT ( 'NONE',  ( 18.00000000000000000, 0.000000000000000000, 0.000000000000000000 ) ) ;
#56529=ORIENTED_EDGE ( 'NONE', *, *, #51176, .T. ) ;
#56596=CARTESIAN_POINT ( 'NONE',  ( 12.00000000000000000, 0.000000000000000000, -31.99999999999998579 ) ) ;
#56659=ORIENTED_EDGE ( 'NONE', *, *, #15516, .T. ) ;
#56720=LINE ( 'NONE', #61994, #56930 ) ;
#56747=CARTESIAN_POINT ( 'NONE',  ( 0.000000000000000000, 0.000000000000000000, -28.00000000000000000 ) ) ;
#56771=AXIS2_PLACEMENT_3D ( 'NONE', #32352, #67419, #73076 ) ;
#56888=CIRCLE ( 'NONE', #26747, 3.999999999999988010 ) ;
#56930=VECTOR ( 'NONE', #27281, 1000.000000000000000 ) ;
#57136=DIRECTION ( 'NONE',  ( -1.000000000000000000, -0.000000000000000000, -0.000000000000000000 ) ) ;
#57207=EDGE_CURVE ( 'NONE', #17422, #8416, #56264, .T. ) ;
#57344=FACE_BOUND ( 'NONE', #61124, .T. ) ;
#57354=AXIS2_PLACEMENT_3D ( 'NONE', #63097, #11422, #34459 ) ;
#57503=CYLINDRICAL_SURFACE ( 'NONE', #59920, 3.999999999999986233 ) ;
#57631=ORIENTED_EDGE ( 'NONE', *, *, #38065, .T. ) ;
#57714=DIRECTION ( 'NONE',  ( 1.000000000000000000, -0.000000000000000000, -0.000000000000000000 ) ) ;
#57767=( LENGTH_UNIT ( ) NAMED_UNIT ( * ) SI_UNIT ( .MILLI., .METRE. ) );
#57835=( LENGTH_UNIT ( ) NAMED_UNIT ( * ) SI_UNIT ( .MILLI., .METRE. ) );
#57920=ADVANCED_FACE ( 'NONE', ( #28675 ), #35102, .F. ) ;
#58184=ORIENTED_EDGE ( 'NONE', *, *, #42763, .T. ) ;
#58259=ORIENTED_EDGE ( 'NONE', *, *, #52568, .F. ) ;
#58271=ORIENTED_EDGE ( 'NONE', *, *, #47955, .T. ) ;
#58738=EDGE_CURVE ( 'NONE', #20975, #17422, #32631, .T. ) ;
#58750=ORIENTED_EDGE ( 'NONE', *, *, #50525, .T. ) ;
#58756=ORIENTED_EDGE ( 'NONE', *, *, #52568, .T. ) ;
#58900=CARTESIAN_POINT ( 'NONE',  ( 17.99999999999998934, 0.000000000000000000, 0.000000000000000000 ) ) ;
#59097=DIRECTION ( 'NONE',  ( 0.000000000000000000, 0.000000000000000000, -1.000000000000000000 ) ) ;
#59130=ADVANCED_FACE ( 'NONE', ( #41495 ), #8265, .F. ) ;
#59143=ORIENTED_EDGE ( 'NONE', *, *, #20102, .T. ) ;
#59460=DIRECTION ( 'NONE',  ( 1.000000000000000000, -0.000000000000000000, -0.000000000000000000 ) ) ;
#59572=CARTESIAN_POINT ( 'NONE',  ( 12.00000000000000000, 0.000000000000000000, -28.00000000000000000 ) ) ;
#59601=( NAMED_UNIT ( * ) PLANE_ANGLE_UNIT ( ) SI_UNIT ( $, .RADIAN. ) );
#59920=AXIS2_PLACEMENT_3D ( 'NONE', #28803, #51821, #17482 ) ;
#60062=FACE_OUTER_BOUND ( 'NONE', #48685, .T. ) ;
#60205=ORIENTED_EDGE ( 'NONE', *, *, #62693, .F. ) ;
#60403=VERTEX_POINT ( 'NONE', #65064 ) ;
#60405=DIRECTION ( 'NONE',  ( 0.000000000000000000, 0.000000000000000000, -1.000000000000000000 ) ) ;
#60410=DIRECTION ( 'NONE',  ( -1.000000000000000000, -0.000000000000000000, -0.000000000000000000 ) ) ;
#60546=EDGE_LOOP ( 'NONE', ( #21694, #21647 ) ) ;
#60568=EDGE_CURVE ( 'NONE', #42810, #45762, #36012, .T. ) ;
#60599=ADVANCED_FACE ( 'NONE', ( #8472, #43927, #9607, #37148, #56006, #66937 ), #38275, .T. ) ;
#60639=ORIENTED_EDGE ( 'NONE', *, *, #28148, .F. ) ;
#60838=ORIENTED_EDGE ( 'NONE', *, *, #42763, .F. ) ;
#60902=CARTESIAN_POINT ( 'NONE',  ( 12.00000000000000000, 0.000000000000000000, 36.00000000000000000 ) ) ;
#60924=CARTESIAN_POINT ( 'NONE',  ( 18.00000000000000000, 0.000000000000000000, 0.000000000000000000 ) ) ;
#61124=EDGE_LOOP ( 'NONE', ( #8064, #40796 ) ) ;
#61125=AXIS2_PLACEMENT_3D ( 'NONE', #29052, #51690, #63009 ) ;
#61271=DIRECTION ( 'NONE',  ( 0.000000000000000000, 0.000000000000000000, 1.000000000000000000 ) ) ;
#61276=ORIENTED_EDGE ( 'NONE', *, *, #54714, .F. ) ;
#61382=DIRECTION ( 'NONE',  ( 1.000000000000000000, -0.000000000000000000, -0.000000000000000000 ) ) ;
#61413=VERTEX_POINT ( 'NONE', #66674 ) ;
#61815=ORIENTED_EDGE ( 'NONE', *, *, #14539, .F. ) ;
#61981=EDGE_CURVE ( 'NONE', #47241, #45978, #1383, .T. ) ;
#61994=CARTESIAN_POINT ( 'NONE',  ( 0.000000000000000000, 1.224646799147352862E-15, -9.999999999999996447 ) ) ;
#62076=CIRCLE ( 'NONE', #63264, 3.999999999999986233 ) ;
#62206=EDGE_CURVE ( 'NONE', #36324, #24263, #35395, .T. ) ;
#62210=CARTESIAN_POINT ( 'NONE',  ( 12.00000000000000000, 28.00000000000000000, 3.999999999999986233 ) ) ;
#62272=AXIS2_PLACEMENT_3D ( 'NONE', #16986, #40013, #63015 ) ;
#62290=DIRECTION ( 'NONE',  ( 0.000000000000000000, 0.000000000000000000, 1.000000000000000000 ) ) ;
#62348=DIRECTION ( 'NONE',  ( 1.000000000000000000, 0.000000000000000000, 0.000000000000000000 ) ) ;
#62589=PRODUCT ( 'spindle bearing', 'spindle bearing', '', ( #22936 ) ) ;
#62608=PLANE ( 'NONE',  #27619 ) ;
#62693=EDGE_CURVE ( 'NONE', #48616, #15213, #15082, .T. ) ;
#62825=EDGE_LOOP ( 'NONE', ( #41592, #59143, #58184, #12870 ) ) ;
#62854=CARTESIAN_POINT ( 'NONE',  ( 12.00000000000000000, -28.00000000000000000, 3.999999999999988010 ) ) ;
#62897=AXIS2_PLACEMENT_3D ( 'NONE', #1464, #24445, #45976 ) ;
#62907=AXIS2_PLACEMENT_3D ( 'NONE', #56300, #21208, #67618 ) ;
#62986=AXIS2_PLACEMENT_3D ( 'NONE', #48858, #8505, #59097 ) ;
#63009=DIRECTION ( 'NONE',  ( 0.000000000000000000, 0.000000000000000000, -1.000000000000000000 ) ) ;
#63015=DIRECTION ( 'NONE',  ( 0.000000000000000000, 0.000000000000000000, 1.000000000000000000 ) ) ;
#63054=EDGE_CURVE ( 'NONE', #66240, #64014, #17275, .T. ) ;
#63063=EDGE_CURVE ( 'NONE', #17476, #5945, #52244, .T. ) ;
#63097=CARTESIAN_POINT ( 'NONE',  ( 0.000000000000000000, 0.000000000000000000, 0.000000000000000000 ) ) ;
#63111=ORIENTED_EDGE ( 'NONE', *, *, #4551, .T. ) ;
#63264=AXIS2_PLACEMENT_3D ( 'NONE', #45426, #57136, #46174 ) ;
#63440=CIRCLE ( 'NONE', #44167, 36.00000000000000000 ) ;
#63708=AXIS2_PLACEMENT_3D ( 'NONE', #56747, #73712, #15242 ) ;
#63805=ORIENTED_EDGE ( 'NONE', *, *, #15005, .T. ) ;
#63819=CARTESIAN_POINT ( 'NONE',  ( 0.000000000000000000, 0.000000000000000000, 28.00000000000000000 ) ) ;
#63997=CARTESIAN_POINT ( 'NONE',  ( 0.000000000000000000, 0.000000000000000000, 19.00000000000000355 ) ) ;
#64014=VERTEX_POINT ( 'NONE', #16400 ) ;
#64341=CARTESIAN_POINT ( 'NONE',  ( 18.00000000000000000, 2.326828918379971365E-15, -19.00000000000000355 ) ) ;
#65064=CARTESIAN_POINT ( 'NONE',  ( 17.99999999999998934, 0.000000000000000000, 9.999999999999996447 ) ) ;
#65089=DIRECTION ( 'NONE',  ( 0.000000000000000000, 0.000000000000000000, 1.000000000000000000 ) ) ;
#65169=CARTESIAN_POINT ( 'NONE',  ( 0.000000000000000000, 4.898587196589400010E-16, 31.99999999999998579 ) ) ;
#65192=CARTESIAN_POINT ( 'NONE',  ( 12.00000000000000178, 4.898587196589402968E-16, -24.00000000000001066 ) ) ;
#65391=UNCERTAINTY_MEASURE_WITH_UNIT (LENGTH_MEASURE( 1.000000000000000082E-05 ), #57767, 'distance_accuracy_value', 'NONE');
#65556=CARTESIAN_POINT ( 'NONE',  ( 0.000000000000000000, -28.00000000000000000, 3.999999999999988010 ) ) ;
#66002=CARTESIAN_POINT ( 'NONE',  ( 0.000000000000000000, 0.000000000000000000, 9.999999999999996447 ) ) ;
#66005=AXIS2_PLACEMENT_3D ( 'NONE', #66095, #49871, #72887 ) ;
#66090=ORIENTED_EDGE ( 'NONE', *, *, #47955, .F. ) ;
#66095=CARTESIAN_POINT ( 'NONE',  ( 0.000000000000000000, 0.000000000000000000, 0.000000000000000000 ) ) ;
#66206=DIRECTION ( 'NONE',  ( 0.000000000000000000, 0.000000000000000000, 1.000000000000000000 ) ) ;
#66240=VERTEX_POINT ( 'NONE', #26913 ) ;
#66520=EDGE_LOOP ( 'NONE', ( #45779, #56659 ) ) ;
#66621=CIRCLE ( 'NONE', #8802, 3.999999999999986233 ) ;
#66654=VECTOR ( 'NONE', #20365, 1000.000000000000000 ) ;
#66674=CARTESIAN_POINT ( 'NONE',  ( 17.99999999999998934, 1.224646799147352862E-15, -9.999999999999996447 ) ) ;
#66794=ORIENTED_EDGE ( 'NONE', *, *, #33685, .T. ) ;
#66937=FACE_OUTER_BOUND ( 'NONE', #53764, .T. ) ;
#67419=DIRECTION ( 'NONE',  ( -1.000000000000000000, -0.000000000000000000, -0.000000000000000000 ) ) ;
#67592=CYLINDRICAL_SURFACE ( 'NONE', #33680, 36.00000000000000000 ) ;
#67598=PRODUCT_DEFINITION ( 'UNKNOWN', '', #12884, #33246 ) ;
#67618=DIRECTION ( 'NONE',  ( 0.000000000000000000, 0.000000000000000000, 1.000000000000000000 ) ) ;
#67734=DIRECTION ( 'NONE',  ( 0.000000000000000000, 0.000000000000000000, -1.000000000000000000 ) ) ;
#67912=LINE ( 'NONE', #5660, #52621 ) ;
#68000=ORIENTED_EDGE ( 'NONE', *, *, #50100, .F. ) ;
#68218=EDGE_LOOP ( 'NONE', ( #21086, #18770 ) ) ;
#68297=CARTESIAN_POINT ( 'NONE',  ( 12.00000000000000000, 28.00000000000000000, 0.000000000000000000 ) ) ;
#68808=CARTESIAN_POINT ( 'NONE',  ( 12.00000000000000000, 0.000000000000000000, 36.00000000000000000 ) ) ;
#68848=ADVANCED_FACE ( 'NONE', ( #29149, #45748 ), #29520, .T. ) ;
#69050=ORIENTED_EDGE ( 'NONE', *, *, #36176, .T. ) ;
#69234=ORIENTED_EDGE ( 'NONE', *, *, #20328, .F. ) ;
#69750=DIRECTION ( 'NONE',  ( 0.000000000000000000, 0.000000000000000000, 1.000000000000000000 ) ) ;
#69766=DIRECTION ( 'NONE',  ( -0.000000000000000000, 0.000000000000000000, 1.000000000000000000 ) ) ;
#69813=LINE ( 'NONE', #13918, #55268 ) ;
#69878=CARTESIAN_POINT ( 'NONE',  ( 11.99999999999999822, 2.326828918379971365E-15, -19.00000000000000355 ) ) ;
#70514=LINE ( 'NONE', #47124, #21584 ) ;
#70702=ORIENTED_EDGE ( 'NONE', *, *, #20102, .F. ) ;
#70853=AXIS2_PLACEMENT_3D ( 'NONE', #451, #46444, #35508 ) ;
#70906=( GEOMETRIC_REPRESENTATION_CONTEXT ( 3 ) GLOBAL_UNCERTAINTY_ASSIGNED_CONTEXT ( ( #65391 ) ) GLOBAL_UNIT_ASSIGNED_CONTEXT ( ( #57767, #59601, #19591 ) ) REPRESENTATION_CONTEXT ( 'NONE', 'WORKASPACE' ) );
#71052=ORIENTED_EDGE ( 'NONE', *, *, #61981, .T. ) ;
#71406=EDGE_LOOP ( 'NONE', ( #16965, #2417 ) ) ;
#71716=DIRECTION ( 'NONE',  ( 1.000000000000000000, -0.000000000000000000, -0.000000000000000000 ) ) ;
#71864=DIRECTION ( 'NONE',  ( 0.000000000000000000, 0.000000000000000000, 1.000000000000000000 ) ) ;
#71941=DIRECTION ( 'NONE',  ( -1.000000000000000000, -0.000000000000000000, -0.000000000000000000 ) ) ;
#72086=STYLED_ITEM('',(#74699),#42707);
#72278=EDGE_CURVE ( 'NONE', #44181, #20642, #62076, .T. ) ;
#72291=DIRECTION ( 'NONE',  ( -1.000000000000000000, -0.000000000000000000, -0.000000000000000000 ) ) ;
#72300=DIRECTION ( 'NONE',  ( 1.000000000000000000, -0.000000000000000000, -0.000000000000000000 ) ) ;
#72327=ORIENTED_EDGE ( 'NONE', *, *, #58738, .T. ) ;
#72351=CARTESIAN_POINT ( 'NONE',  ( 11.99999999999999822, 0.000000000000000000, 19.00000000000000355 ) ) ;
#72363=AXIS2_PLACEMENT_3D ( 'NONE', #52303, #639, #17963 ) ;
#72450=CARTESIAN_POINT ( 'NONE',  ( 12.00000000000000178, 0.000000000000000000, -28.00000000000000000 ) ) ;
#72549=ORIENTED_EDGE ( 'NONE', *, *, #62206, .T. ) ;
#72814=ORIENTED_EDGE ( 'NONE', *, *, #3794, .T. ) ;
#72832=CIRCLE ( 'NONE', #42704, 3.999999999999986233 ) ;
#72887=DIRECTION ( 'NONE',  ( 0.000000000000000000, 0.000000000000000000, 1.000000000000000000 ) ) ;
#72941=ORIENTED_EDGE ( 'NONE', *, *, #12299, .F. ) ;
#73076=DIRECTION ( 'NONE',  ( 0.000000000000000000, 0.000000000000000000, 1.000000000000000000 ) ) ;
#73166=CIRCLE ( 'NONE', #51457, 9.999999999999996447 ) ;
#73237=ORIENTED_EDGE ( 'NONE', *, *, #21071, .F. ) ;
#73274=ORIENTED_EDGE ( 'NONE', *, *, #45739, .T. ) ;
#73328=AXIS2_PLACEMENT_3D ( 'NONE', #60902, #55635, #48829 ) ;
#73712=DIRECTION ( 'NONE',  ( -1.000000000000000000, -0.000000000000000000, -0.000000000000000000 ) ) ;
#73717=AXIS2_PLACEMENT_3D ( 'NONE', #63819, #34806, #18908 ) ;
#74031=DIRECTION ( 'NONE',  ( -1.000000000000000000, -0.000000000000000000, -0.000000000000000000 ) ) ;
#74466=ORIENTED_EDGE ( 'NONE', *, *, #54048, .F. ) ;
#74693=COLOUR_RGB('Grey',0.48,0.52,0.57);
#74694=FILL_AREA_STYLE_COLOUR('',#74693);
#74695=FILL_AREA_STYLE('',(#74694));
#74696=SURFACE_STYLE_FILL_AREA(#74695);
#74697=SURFACE_SIDE_STYLE('',(#74696));
#74698=SURFACE_STYLE_USAGE(.BOTH.,#74697);
#74699=PRESENTATION_STYLE_ASSIGNMENT((#74698));
ENDSEC;
END-ISO-10303-21;
